ISO-10303-21;
HEADER;
/* Generated by software containing ST-Developer
 * from STEP Tools, Inc. (www.steptools.com) 
 */

FILE_DESCRIPTION(
/* description */ ('Line shaft on three pillow blocks'),
/* implementation_level */ '2;1');

FILE_NAME(
/* name */ 'Bonded foot pad (1).step',
/* time_stamp */ '2026-10-27T10:49:19-07:00',
/* author */ (''),
/* organization */ (''),
/* preprocessor_version */ 'ST-DEVELOPER v20.2',
/* originating_system */ 'Autodesk Translation Framework v15.17.0.0',
/* authorisation */ '');

FILE_SCHEMA (('AUTOMOTIVE_DESIGN { 1 0 10303 214 3 1 1 }'));
ENDSEC;

DATA;
#10=MECHANICAL_DESIGN_GEOMETRIC_PRESENTATION_REPRESENTATION('',(#342),#8377);
#288=SHAPE_REPRESENTATION_RELATIONSHIP('SRR','None',#8503,#315);
#315=ADVANCED_BREP_SHAPE_REPRESENTATION('',(#370),#8352);
#342=STYLED_ITEM('',(#8711),#370);
#370=MANIFOLD_SOLID_BREP('Body1',#4328);
#516=PLANE('',#4730);
#517=PLANE('',#4731);
#518=PLANE('',#4732);
#519=PLANE('',#4733);
#520=PLANE('',#4734);
#521=PLANE('',#4735);
#696=FACE_OUTER_BOUND('',#972,.T.);
#697=FACE_OUTER_BOUND('',#973,.T.);
#698=FACE_OUTER_BOUND('',#974,.T.);
#699=FACE_OUTER_BOUND('',#975,.T.);
#700=FACE_OUTER_BOUND('',#976,.T.);
#701=FACE_OUTER_BOUND('',#977,.T.);
#972=EDGE_LOOP('',(#3129,#3130,#3131,#3132));
#973=EDGE_LOOP('',(#3133,#3134,#3135,#3136));
#974=EDGE_LOOP('',(#3137,#3138,#3139,#3140));
#975=EDGE_LOOP('',(#3141,#3142,#3143,#3144));
#976=EDGE_LOOP('',(#3145,#3146,#3147,#3148));
#977=EDGE_LOOP('',(#3149,#3150,#3151,#3152));
#1317=LINE('',#6667,#1644);
#1318=LINE('',#6669,#1645);
#1319=LINE('',#6671,#1646);
#1320=LINE('',#6672,#1647);
#1321=LINE('',#6675,#1648);
#1322=LINE('',#6677,#1649);
#1323=LINE('',#6678,#1650);
#1324=LINE('',#6681,#1651);
#1325=LINE('',#6683,#1652);
#1326=LINE('',#6684,#1653);
#1327=LINE('',#6686,#1654);
#1328=LINE('',#6687,#1655);
#1644=VECTOR('',#5366,1.);
#1645=VECTOR('',#5367,1.);
#1646=VECTOR('',#5368,1.);
#1647=VECTOR('',#5369,1.);
#1648=VECTOR('',#5372,1.);
#1649=VECTOR('',#5373,1.);
#1650=VECTOR('',#5374,1.);
#1651=VECTOR('',#5377,1.);
#1652=VECTOR('',#5378,1.);
#1653=VECTOR('',#5379,1.);
#1654=VECTOR('',#5382,1.);
#1655=VECTOR('',#5383,1.);
#2128=VERTEX_POINT('',#6665);
#2129=VERTEX_POINT('',#6666);
#2130=VERTEX_POINT('',#6668);
#2131=VERTEX_POINT('',#6670);
#2132=VERTEX_POINT('',#6674);
#2133=VERTEX_POINT('',#6676);
#2134=VERTEX_POINT('',#6680);
#2135=VERTEX_POINT('',#6682);
#2513=EDGE_CURVE('',#2128,#2129,#1317,.T.);
#2514=EDGE_CURVE('',#2129,#2130,#1318,.T.);
#2515=EDGE_CURVE('',#2131,#2130,#1319,.T.);
#2516=EDGE_CURVE('',#2128,#2131,#1320,.T.);
#2517=EDGE_CURVE('',#2132,#2128,#1321,.T.);
#2518=EDGE_CURVE('',#2133,#2131,#1322,.T.);
#2519=EDGE_CURVE('',#2132,#2133,#1323,.T.);
#2520=EDGE_CURVE('',#2134,#2132,#1324,.T.);
#2521=EDGE_CURVE('',#2135,#2133,#1325,.T.);
#2522=EDGE_CURVE('',#2134,#2135,#1326,.T.);
#2523=EDGE_CURVE('',#2129,#2134,#1327,.T.);
#2524=EDGE_CURVE('',#2130,#2135,#1328,.T.);
#3129=ORIENTED_EDGE('',*,*,#2513,.T.);
#3130=ORIENTED_EDGE('',*,*,#2514,.T.);
#3131=ORIENTED_EDGE('',*,*,#2515,.F.);
#3132=ORIENTED_EDGE('',*,*,#2516,.F.);
#3133=ORIENTED_EDGE('',*,*,#2517,.T.);
#3134=ORIENTED_EDGE('',*,*,#2516,.T.);
#3135=ORIENTED_EDGE('',*,*,#2518,.F.);
#3136=ORIENTED_EDGE('',*,*,#2519,.F.);
#3137=ORIENTED_EDGE('',*,*,#2520,.T.);
#3138=ORIENTED_EDGE('',*,*,#2519,.T.);
#3139=ORIENTED_EDGE('',*,*,#2521,.F.);
#3140=ORIENTED_EDGE('',*,*,#2522,.F.);
#3141=ORIENTED_EDGE('',*,*,#2523,.T.);
#3142=ORIENTED_EDGE('',*,*,#2522,.T.);
#3143=ORIENTED_EDGE('',*,*,#2524,.F.);
#3144=ORIENTED_EDGE('',*,*,#2514,.F.);
#3145=ORIENTED_EDGE('',*,*,#2524,.T.);
#3146=ORIENTED_EDGE('',*,*,#2521,.T.);
#3147=ORIENTED_EDGE('',*,*,#2518,.T.);
#3148=ORIENTED_EDGE('',*,*,#2515,.T.);
#3149=ORIENTED_EDGE('',*,*,#2523,.F.);
#3150=ORIENTED_EDGE('',*,*,#2513,.F.);
#3151=ORIENTED_EDGE('',*,*,#2517,.F.);
#3152=ORIENTED_EDGE('',*,*,#2520,.F.);
#4114=ADVANCED_FACE('',(#696),#516,.T.);
#4115=ADVANCED_FACE('',(#697),#517,.T.);
#4116=ADVANCED_FACE('',(#698),#518,.T.);
#4117=ADVANCED_FACE('',(#699),#519,.T.);
#4118=ADVANCED_FACE('',(#700),#520,.T.);
#4119=ADVANCED_FACE('',(#701),#521,.F.);
#4328=CLOSED_SHELL('',(#4114,#4115,#4116,#4117,#4118,#4119));
#4729=AXIS2_PLACEMENT_3D('',#6663,#5362,#5363);
#4730=AXIS2_PLACEMENT_3D('',#6664,#5364,#5365);
#4731=AXIS2_PLACEMENT_3D('',#6673,#5370,#5371);
#4732=AXIS2_PLACEMENT_3D('',#6679,#5375,#5376);
#4733=AXIS2_PLACEMENT_3D('',#6685,#5380,#5381);
#4734=AXIS2_PLACEMENT_3D('',#6688,#5384,#5385);
#4735=AXIS2_PLACEMENT_3D('',#6689,#5386,#5387);
#5362=DIRECTION('axis',(0.,0.,1.));
#5363=DIRECTION('refdir',(1.,0.,0.));
#5364=DIRECTION('center_axis',(0.,1.,0.));
#5365=DIRECTION('ref_axis',(-1.,0.,0.));
#5366=DIRECTION('',(-1.,0.,0.));
#5367=DIRECTION('',(0.,0.,1.));
#5368=DIRECTION('',(-1.,0.,0.));
#5369=DIRECTION('',(0.,0.,1.));
#5370=DIRECTION('center_axis',(1.,0.,0.));
#5371=DIRECTION('ref_axis',(0.,1.,0.));
#5372=DIRECTION('',(0.,1.,0.));
#5373=DIRECTION('',(0.,1.,0.));
#5374=DIRECTION('',(0.,0.,1.));
#5375=DIRECTION('center_axis',(0.,-1.,0.));
#5376=DIRECTION('ref_axis',(1.,0.,0.));
#5377=DIRECTION('',(1.,0.,0.));
#5378=DIRECTION('',(1.,0.,0.));
#5379=DIRECTION('',(0.,0.,1.));
#5380=DIRECTION('center_axis',(-1.,0.,0.));
#5381=DIRECTION('ref_axis',(0.,-1.,0.));
#5382=DIRECTION('',(0.,-1.,0.));
#5383=DIRECTION('',(0.,-1.,0.));
#5384=DIRECTION('center_axis',(0.,0.,1.));
#5385=DIRECTION('ref_axis',(1.,0.,0.));
#5386=DIRECTION('center_axis',(0.,0.,1.));
#5387=DIRECTION('ref_axis',(1.,0.,0.));
#6663=CARTESIAN_POINT('',(0.,0.,0.));
#6664=CARTESIAN_POINT('Origin',(9.,34.,-1.8));
#6665=CARTESIAN_POINT('',(9.,34.,-1.8));
#6666=CARTESIAN_POINT('',(-9.,34.,-1.8));
#6667=CARTESIAN_POINT('',(9.,34.,-1.8));
#6668=CARTESIAN_POINT('',(-9.,34.,-1.5));
#6669=CARTESIAN_POINT('',(-9.,34.,-1.8));
#6670=CARTESIAN_POINT('',(9.,34.,-1.5));
#6671=CARTESIAN_POINT('',(9.,34.,-1.5));
#6672=CARTESIAN_POINT('',(9.,34.,-1.8));
#6673=CARTESIAN_POINT('Origin',(9.,32.,-1.8));
#6674=CARTESIAN_POINT('',(9.,32.,-1.8));
#6675=CARTESIAN_POINT('',(9.,32.,-1.8));
#6676=CARTESIAN_POINT('',(9.,32.,-1.5));
#6677=CARTESIAN_POINT('',(9.,32.,-1.5));
#6678=CARTESIAN_POINT('',(9.,32.,-1.8));
#6679=CARTESIAN_POINT('Origin',(-9.,32.,-1.8));
#6680=CARTESIAN_POINT('',(-9.,32.,-1.8));
#6681=CARTESIAN_POINT('',(-9.,32.,-1.8));
#6682=CARTESIAN_POINT('',(-9.,32.,-1.5));
#6683=CARTESIAN_POINT('',(-9.,32.,-1.5));
#6684=CARTESIAN_POINT('',(-9.,32.,-1.8));
#6685=CARTESIAN_POINT('Origin',(-9.,34.,-1.8));
#6686=CARTESIAN_POINT('',(-9.,34.,-1.8));
#6687=CARTESIAN_POINT('',(-9.,34.,-1.5));
#6688=CARTESIAN_POINT('Origin',(0.,33.,-1.5));
#6689=CARTESIAN_POINT('Origin',(0.,33.,-1.8));
#8320=UNCERTAINTY_MEASURE_WITH_UNIT(LENGTH_MEASURE(0.001),#8378,
'DISTANCE_ACCURACY_VALUE',
'Maximum model space distance between geometric entities at asserted c
onnectivities');
#8345=UNCERTAINTY_MEASURE_WITH_UNIT(LENGTH_MEASURE(0.001),#8378,
'DISTANCE_ACCURACY_VALUE',
'Maximum model space distance between geometric entities at asserted c
onnectivities');
#8352=(
GEOMETRIC_REPRESENTATION_CONTEXT(3)
GLOBAL_UNCERTAINTY_ASSIGNED_CONTEXT((#8320))
GLOBAL_UNIT_ASSIGNED_CONTEXT((#8378,#8380,#8381))
REPRESENTATION_CONTEXT('','3D')
);
#8377=(
GEOMETRIC_REPRESENTATION_CONTEXT(3)
GLOBAL_UNCERTAINTY_ASSIGNED_CONTEXT((#8345))
GLOBAL_UNIT_ASSIGNED_CONTEXT((#8378,#8380,#8381))
REPRESENTATION_CONTEXT('','3D')
);
#8378=(
LENGTH_UNIT()
NAMED_UNIT(*)
SI_UNIT(.CENTI.,.METRE.)
);
#8380=(
NAMED_UNIT(*)
PLANE_ANGLE_UNIT()
SI_UNIT($,.RADIAN.)
);
#8381=(
NAMED_UNIT(*)
SI_UNIT($,.STERADIAN.)
SOLID_ANGLE_UNIT()
);
#8388=SHAPE_DEFINITION_REPRESENTATION(#8419,#8503);
#8419=PRODUCT_DEFINITION_SHAPE('',$,#8535);
#8503=SHAPE_REPRESENTATION('',(#4729),#8352);
#8528=PRODUCT_DEFINITION_CONTEXT('part definition',#8623,'design');
#8535=PRODUCT_DEFINITION('Bonded foot pad (1)','Bonded foot pad (1)',#8566,
#8528);
#8566=PRODUCT_DEFINITION_FORMATION('',$,#8631);
#8623=APPLICATION_CONTEXT(
'Core Data for Automotive Mechanical Design Process');
#8624=PRODUCT_CONTEXT('part definition',#8623,'mechanical');
#8631=PRODUCT('Bonded foot pad (1)','Bonded foot pad (1)',
'Bonded foot pad (1)',(#8624));
#8705=COLOUR_RGB('Sky Blue',0.24,0.69,0.87);
#8706=FILL_AREA_STYLE_COLOUR('',#8705);
#8707=FILL_AREA_STYLE('',(#8706));
#8708=SURFACE_STYLE_FILL_AREA(#8707);
#8709=SURFACE_SIDE_STYLE('',(#8708));
#8710=SURFACE_STYLE_USAGE(.BOTH.,#8709);
#8711=PRESENTATION_STYLE_ASSIGNMENT((#8710));
ENDSEC;
END-ISO-10303-21;
